ISO-10303-21;
HEADER;
/* Generated by software containing ST-Developer
 * from STEP Tools, Inc. (www.steptools.com) 
 */

FILE_DESCRIPTION(
/* description */ ('XY cross-slide table'),
/* implementation_level */ '2;1');

FILE_NAME(
/* name */ 'M5x30 frame screw.step',
/* time_stamp */ '2026-10-28T03:22:46-07:00',
/* author */ (''),
/* organization */ (''),
/* preprocessor_version */ 'ST-DEVELOPER v20.2',
/* originating_system */ 'Autodesk Translation Framework v15.17.0.0',
/* authorisation */ '');

FILE_SCHEMA (('AUTOMOTIVE_DESIGN { 1 0 10303 214 3 1 1 }'));
ENDSEC;

DATA;
#10=MECHANICAL_DESIGN_GEOMETRIC_PRESENTATION_REPRESENTATION('',(#1713),#62984);
#19=ORIENTED_CLOSED_SHELL('',*,#23007,.F.);
#28=BREP_WITH_VOIDS('Body1',#23008,(#19));
#1450=CONICAL_SURFACE('',#24741,0.4,0.785398163397448);
#1451=CONICAL_SURFACE('',#24745,0.41,0.785398163397448);
#1452=CONICAL_SURFACE('',#24749,0.26,0.463647609000806);
#1532=SHAPE_REPRESENTATION_RELATIONSHIP('SRR','None',#63384,#1615);
#1615=ADVANCED_BREP_SHAPE_REPRESENTATION('',(#28),#62921);
#1713=STYLED_ITEM('',(#63919),#28);
#2048=FACE_BOUND('',#4695,.T.);
#2049=FACE_BOUND('',#4703,.T.);
#2479=PLANE('',#24725);
#2480=PLANE('',#24726);
#2481=PLANE('',#24727);
#2482=PLANE('',#24728);
#2483=PLANE('',#24729);
#2484=PLANE('',#24730);
#2485=PLANE('',#24731);
#2486=PLANE('',#24732);
#2487=PLANE('',#24733);
#2488=PLANE('',#24738);
#2489=PLANE('',#24739);
#2490=PLANE('',#24747);
#3211=FACE_OUTER_BOUND('',#4686,.T.);
#3212=FACE_OUTER_BOUND('',#4687,.T.);
#3213=FACE_OUTER_BOUND('',#4688,.T.);
#3214=FACE_OUTER_BOUND('',#4689,.T.);
#3215=FACE_OUTER_BOUND('',#4690,.T.);
#3216=FACE_OUTER_BOUND('',#4691,.T.);
#3217=FACE_OUTER_BOUND('',#4692,.T.);
#3218=FACE_OUTER_BOUND('',#4693,.T.);
#3219=FACE_OUTER_BOUND('',#4694,.T.);
#3220=FACE_OUTER_BOUND('',#4696,.T.);
#3221=FACE_OUTER_BOUND('',#4697,.T.);
#3222=FACE_OUTER_BOUND('',#4698,.T.);
#3223=FACE_OUTER_BOUND('',#4699,.T.);
#3224=FACE_OUTER_BOUND('',#4700,.T.);
#3225=FACE_OUTER_BOUND('',#4701,.T.);
#3226=FACE_OUTER_BOUND('',#4702,.T.);
#3227=FACE_OUTER_BOUND('',#4704,.T.);
#3228=FACE_OUTER_BOUND('',#4705,.T.);
#4686=EDGE_LOOP('',(#16436,#16437,#16438,#16439));
#4687=EDGE_LOOP('',(#16440,#16441,#16442,#16443));
#4688=EDGE_LOOP('',(#16444,#16445,#16446,#16447));
#4689=EDGE_LOOP('',(#16448,#16449,#16450,#16451));
#4690=EDGE_LOOP('',(#16452,#16453,#16454,#16455));
#4691=EDGE_LOOP('',(#16456,#16457,#16458,#16459));
#4692=EDGE_LOOP('',(#16460,#16461,#16462,#16463,#16464,#16465));
#4693=EDGE_LOOP('',(#16466,#16467,#16468,#16469,#16470,#16471));
#4694=EDGE_LOOP('',(#16472));
#4695=EDGE_LOOP('',(#16473));
#4696=EDGE_LOOP('',(#16474,#16475,#16476,#16477));
#4697=EDGE_LOOP('',(#16478));
#4698=EDGE_LOOP('',(#16479));
#4699=EDGE_LOOP('',(#16480,#16481,#16482,#16483));
#4700=EDGE_LOOP('',(#16484,#16485,#16486,#16487));
#4701=EDGE_LOOP('',(#16488,#16489,#16490,#16491));
#4702=EDGE_LOOP('',(#16492));
#4703=EDGE_LOOP('',(#16493));
#4704=EDGE_LOOP('',(#16494,#16495,#16496,#16497));
#4705=EDGE_LOOP('',(#16498,#16499,#16500,#16501));
#6306=LINE('',#35187,#7793);
#6307=LINE('',#35189,#7794);
#6308=LINE('',#35191,#7795);
#6309=LINE('',#35192,#7796);
#6310=LINE('',#35195,#7797);
#6311=LINE('',#35197,#7798);
#6312=LINE('',#35198,#7799);
#6313=LINE('',#35201,#7800);
#6314=LINE('',#35203,#7801);
#6315=LINE('',#35204,#7802);
#6316=LINE('',#35207,#7803);
#6317=LINE('',#35209,#7804);
#6318=LINE('',#35210,#7805);
#6319=LINE('',#35213,#7806);
#6320=LINE('',#35215,#7807);
#6321=LINE('',#35216,#7808);
#6322=LINE('',#35218,#7809);
#6323=LINE('',#35219,#7810);
#6324=LINE('',#35229,#7811);
#6325=LINE('',#35238,#7812);
#6326=LINE('',#35242,#7813);
#6327=LINE('',#35246,#7814);
#6328=LINE('',#35253,#7815);
#6329=LINE('',#35255,#7816);
#7793=VECTOR('',#28313,1.);
#7794=VECTOR('',#28314,1.);
#7795=VECTOR('',#28315,1.);
#7796=VECTOR('',#28316,1.);
#7797=VECTOR('',#28319,1.);
#7798=VECTOR('',#28320,1.);
#7799=VECTOR('',#28321,1.);
#7800=VECTOR('',#28324,1.);
#7801=VECTOR('',#28325,1.);
#7802=VECTOR('',#28326,1.);
#7803=VECTOR('',#28329,1.);
#7804=VECTOR('',#28330,1.);
#7805=VECTOR('',#28331,1.);
#7806=VECTOR('',#28334,1.);
#7807=VECTOR('',#28335,1.);
#7808=VECTOR('',#28336,1.);
#7809=VECTOR('',#28339,1.);
#7810=VECTOR('',#28340,1.);
#7811=VECTOR('',#28353,0.25);
#7812=VECTOR('',#28366,0.4);
#7813=VECTOR('',#28371,0.425);
#7814=VECTOR('',#28376,0.41);
#7815=VECTOR('',#28385,0.26);
#7816=VECTOR('',#28388,0.25);
#9214=CIRCLE('',#24734,0.25);
#9215=CIRCLE('',#24735,0.24505);
#9216=CIRCLE('',#24737,0.25);
#9217=CIRCLE('',#24740,0.375);
#9218=CIRCLE('',#24742,0.425);
#9219=CIRCLE('',#24744,0.425);
#9220=CIRCLE('',#24746,0.395);
#9221=CIRCLE('',#24748,0.27);
#9222=CIRCLE('',#24750,0.24505);
#10298=VERTEX_POINT('',#35185);
#10299=VERTEX_POINT('',#35186);
#10300=VERTEX_POINT('',#35188);
#10301=VERTEX_POINT('',#35190);
#10302=VERTEX_POINT('',#35194);
#10303=VERTEX_POINT('',#35196);
#10304=VERTEX_POINT('',#35200);
#10305=VERTEX_POINT('',#35202);
#10306=VERTEX_POINT('',#35206);
#10307=VERTEX_POINT('',#35208);
#10308=VERTEX_POINT('',#35212);
#10309=VERTEX_POINT('',#35214);
#10310=VERTEX_POINT('',#35223);
#10311=VERTEX_POINT('',#35225);
#10312=VERTEX_POINT('',#35228);
#10313=VERTEX_POINT('',#35233);
#10314=VERTEX_POINT('',#35236);
#10315=VERTEX_POINT('',#35240);
#10316=VERTEX_POINT('',#35244);
#10317=VERTEX_POINT('',#35248);
#10318=VERTEX_POINT('',#35251);
#12602=EDGE_CURVE('',#10298,#10299,#6306,.T.);
#12603=EDGE_CURVE('',#10299,#10300,#6307,.T.);
#12604=EDGE_CURVE('',#10300,#10301,#6308,.T.);
#12605=EDGE_CURVE('',#10298,#10301,#6309,.T.);
#12606=EDGE_CURVE('',#10299,#10302,#6310,.T.);
#12607=EDGE_CURVE('',#10302,#10303,#6311,.T.);
#12608=EDGE_CURVE('',#10303,#10300,#6312,.T.);
#12609=EDGE_CURVE('',#10302,#10304,#6313,.T.);
#12610=EDGE_CURVE('',#10304,#10305,#6314,.T.);
#12611=EDGE_CURVE('',#10305,#10303,#6315,.T.);
#12612=EDGE_CURVE('',#10304,#10306,#6316,.T.);
#12613=EDGE_CURVE('',#10306,#10307,#6317,.T.);
#12614=EDGE_CURVE('',#10307,#10305,#6318,.T.);
#12615=EDGE_CURVE('',#10306,#10308,#6319,.T.);
#12616=EDGE_CURVE('',#10308,#10309,#6320,.T.);
#12617=EDGE_CURVE('',#10309,#10307,#6321,.T.);
#12618=EDGE_CURVE('',#10308,#10298,#6322,.T.);
#12619=EDGE_CURVE('',#10301,#10309,#6323,.T.);
#12620=EDGE_CURVE('',#10310,#10310,#9214,.T.);
#12621=EDGE_CURVE('',#10311,#10311,#9215,.T.);
#12622=EDGE_CURVE('',#10310,#10312,#6324,.T.);
#12623=EDGE_CURVE('',#10312,#10312,#9216,.T.);
#12624=EDGE_CURVE('',#10313,#10313,#9217,.T.);
#12625=EDGE_CURVE('',#10314,#10314,#9218,.T.);
#12626=EDGE_CURVE('',#10314,#10313,#6325,.T.);
#12627=EDGE_CURVE('',#10315,#10315,#9219,.T.);
#12628=EDGE_CURVE('',#10315,#10314,#6326,.T.);
#12629=EDGE_CURVE('',#10316,#10316,#9220,.T.);
#12630=EDGE_CURVE('',#10316,#10315,#6327,.T.);
#12631=EDGE_CURVE('',#10317,#10317,#9221,.T.);
#12632=EDGE_CURVE('',#10318,#10318,#9222,.F.);
#12633=EDGE_CURVE('',#10318,#10317,#6328,.T.);
#12634=EDGE_CURVE('',#10311,#10318,#6329,.T.);
#16436=ORIENTED_EDGE('',*,*,#12602,.T.);
#16437=ORIENTED_EDGE('',*,*,#12603,.T.);
#16438=ORIENTED_EDGE('',*,*,#12604,.T.);
#16439=ORIENTED_EDGE('',*,*,#12605,.F.);
#16440=ORIENTED_EDGE('',*,*,#12606,.T.);
#16441=ORIENTED_EDGE('',*,*,#12607,.T.);
#16442=ORIENTED_EDGE('',*,*,#12608,.T.);
#16443=ORIENTED_EDGE('',*,*,#12603,.F.);
#16444=ORIENTED_EDGE('',*,*,#12609,.T.);
#16445=ORIENTED_EDGE('',*,*,#12610,.T.);
#16446=ORIENTED_EDGE('',*,*,#12611,.T.);
#16447=ORIENTED_EDGE('',*,*,#12607,.F.);
#16448=ORIENTED_EDGE('',*,*,#12612,.T.);
#16449=ORIENTED_EDGE('',*,*,#12613,.T.);
#16450=ORIENTED_EDGE('',*,*,#12614,.T.);
#16451=ORIENTED_EDGE('',*,*,#12610,.F.);
#16452=ORIENTED_EDGE('',*,*,#12615,.T.);
#16453=ORIENTED_EDGE('',*,*,#12616,.T.);
#16454=ORIENTED_EDGE('',*,*,#12617,.T.);
#16455=ORIENTED_EDGE('',*,*,#12613,.F.);
#16456=ORIENTED_EDGE('',*,*,#12618,.T.);
#16457=ORIENTED_EDGE('',*,*,#12605,.T.);
#16458=ORIENTED_EDGE('',*,*,#12619,.T.);
#16459=ORIENTED_EDGE('',*,*,#12616,.F.);
#16460=ORIENTED_EDGE('',*,*,#12618,.F.);
#16461=ORIENTED_EDGE('',*,*,#12615,.F.);
#16462=ORIENTED_EDGE('',*,*,#12612,.F.);
#16463=ORIENTED_EDGE('',*,*,#12609,.F.);
#16464=ORIENTED_EDGE('',*,*,#12606,.F.);
#16465=ORIENTED_EDGE('',*,*,#12602,.F.);
#16466=ORIENTED_EDGE('',*,*,#12619,.F.);
#16467=ORIENTED_EDGE('',*,*,#12604,.F.);
#16468=ORIENTED_EDGE('',*,*,#12608,.F.);
#16469=ORIENTED_EDGE('',*,*,#12611,.F.);
#16470=ORIENTED_EDGE('',*,*,#12614,.F.);
#16471=ORIENTED_EDGE('',*,*,#12617,.F.);
#16472=ORIENTED_EDGE('',*,*,#12620,.T.);
#16473=ORIENTED_EDGE('',*,*,#12621,.F.);
#16474=ORIENTED_EDGE('',*,*,#12620,.F.);
#16475=ORIENTED_EDGE('',*,*,#12622,.T.);
#16476=ORIENTED_EDGE('',*,*,#12623,.T.);
#16477=ORIENTED_EDGE('',*,*,#12622,.F.);
#16478=ORIENTED_EDGE('',*,*,#12623,.F.);
#16479=ORIENTED_EDGE('',*,*,#12624,.F.);
#16480=ORIENTED_EDGE('',*,*,#12625,.F.);
#16481=ORIENTED_EDGE('',*,*,#12626,.T.);
#16482=ORIENTED_EDGE('',*,*,#12624,.T.);
#16483=ORIENTED_EDGE('',*,*,#12626,.F.);
#16484=ORIENTED_EDGE('',*,*,#12627,.F.);
#16485=ORIENTED_EDGE('',*,*,#12628,.T.);
#16486=ORIENTED_EDGE('',*,*,#12625,.T.);
#16487=ORIENTED_EDGE('',*,*,#12628,.F.);
#16488=ORIENTED_EDGE('',*,*,#12629,.F.);
#16489=ORIENTED_EDGE('',*,*,#12630,.T.);
#16490=ORIENTED_EDGE('',*,*,#12627,.T.);
#16491=ORIENTED_EDGE('',*,*,#12630,.F.);
#16492=ORIENTED_EDGE('',*,*,#12629,.T.);
#16493=ORIENTED_EDGE('',*,*,#12631,.F.);
#16494=ORIENTED_EDGE('',*,*,#12632,.F.);
#16495=ORIENTED_EDGE('',*,*,#12633,.T.);
#16496=ORIENTED_EDGE('',*,*,#12631,.T.);
#16497=ORIENTED_EDGE('',*,*,#12633,.F.);
#16498=ORIENTED_EDGE('',*,*,#12621,.T.);
#16499=ORIENTED_EDGE('',*,*,#12634,.T.);
#16500=ORIENTED_EDGE('',*,*,#12632,.T.);
#16501=ORIENTED_EDGE('',*,*,#12634,.F.);
#21156=CYLINDRICAL_SURFACE('',#24736,0.25);
#21157=CYLINDRICAL_SURFACE('',#24743,0.425);
#21158=CYLINDRICAL_SURFACE('',#24751,0.24505);
#21992=ADVANCED_FACE('',(#3211),#2479,.F.);
#21993=ADVANCED_FACE('',(#3212),#2480,.F.);
#21994=ADVANCED_FACE('',(#3213),#2481,.F.);
#21995=ADVANCED_FACE('',(#3214),#2482,.F.);
#21996=ADVANCED_FACE('',(#3215),#2483,.F.);
#21997=ADVANCED_FACE('',(#3216),#2484,.F.);
#21998=ADVANCED_FACE('',(#3217),#2485,.F.);
#21999=ADVANCED_FACE('',(#3218),#2486,.F.);
#22000=ADVANCED_FACE('',(#3219,#2048),#2487,.T.);
#22001=ADVANCED_FACE('',(#3220),#21156,.T.);
#22002=ADVANCED_FACE('',(#3221),#2488,.F.);
#22003=ADVANCED_FACE('',(#3222),#2489,.T.);
#22004=ADVANCED_FACE('',(#3223),#1450,.T.);
#22005=ADVANCED_FACE('',(#3224),#21157,.T.);
#22006=ADVANCED_FACE('',(#3225),#1451,.T.);
#22007=ADVANCED_FACE('',(#3226,#2049),#2490,.T.);
#22008=ADVANCED_FACE('',(#3227),#1452,.T.);
#22009=ADVANCED_FACE('',(#3228),#21158,.T.);
#23007=CLOSED_SHELL('',(#21992,#21993,#21994,#21995,#21996,#21997,#21998,
#21999));
#23008=CLOSED_SHELL('',(#22000,#22001,#22002,#22003,#22004,#22005,#22006,
#22007,#22008,#22009));
#24724=AXIS2_PLACEMENT_3D('',#35183,#28309,#28310);
#24725=AXIS2_PLACEMENT_3D('',#35184,#28311,#28312);
#24726=AXIS2_PLACEMENT_3D('',#35193,#28317,#28318);
#24727=AXIS2_PLACEMENT_3D('',#35199,#28322,#28323);
#24728=AXIS2_PLACEMENT_3D('',#35205,#28327,#28328);
#24729=AXIS2_PLACEMENT_3D('',#35211,#28332,#28333);
#24730=AXIS2_PLACEMENT_3D('',#35217,#28337,#28338);
#24731=AXIS2_PLACEMENT_3D('',#35220,#28341,#28342);
#24732=AXIS2_PLACEMENT_3D('',#35221,#28343,#28344);
#24733=AXIS2_PLACEMENT_3D('',#35222,#28345,#28346);
#24734=AXIS2_PLACEMENT_3D('',#35224,#28347,#28348);
#24735=AXIS2_PLACEMENT_3D('',#35226,#28349,#28350);
#24736=AXIS2_PLACEMENT_3D('',#35227,#28351,#28352);
#24737=AXIS2_PLACEMENT_3D('',#35230,#28354,#28355);
#24738=AXIS2_PLACEMENT_3D('',#35231,#28356,#28357);
#24739=AXIS2_PLACEMENT_3D('',#35232,#28358,#28359);
#24740=AXIS2_PLACEMENT_3D('',#35234,#28360,#28361);
#24741=AXIS2_PLACEMENT_3D('',#35235,#28362,#28363);
#24742=AXIS2_PLACEMENT_3D('',#35237,#28364,#28365);
#24743=AXIS2_PLACEMENT_3D('',#35239,#28367,#28368);
#24744=AXIS2_PLACEMENT_3D('',#35241,#28369,#28370);
#24745=AXIS2_PLACEMENT_3D('',#35243,#28372,#28373);
#24746=AXIS2_PLACEMENT_3D('',#35245,#28374,#28375);
#24747=AXIS2_PLACEMENT_3D('',#35247,#28377,#28378);
#24748=AXIS2_PLACEMENT_3D('',#35249,#28379,#28380);
#24749=AXIS2_PLACEMENT_3D('',#35250,#28381,#28382);
#24750=AXIS2_PLACEMENT_3D('',#35252,#28383,#28384);
#24751=AXIS2_PLACEMENT_3D('',#35254,#28386,#28387);
#28309=DIRECTION('axis',(0.,0.,1.));
#28310=DIRECTION('refdir',(1.,0.,0.));
#28311=DIRECTION('center_axis',(0.866025403784439,0.,-0.5));
#28312=DIRECTION('ref_axis',(0.5,0.,0.866025403784439));
#28313=DIRECTION('',(-0.5,0.,-0.866025403784439));
#28314=DIRECTION('',(0.,-1.,0.));
#28315=DIRECTION('',(0.5,0.,0.866025403784439));
#28316=DIRECTION('',(0.,-1.,0.));
#28317=DIRECTION('center_axis',(1.20185167898973E-16,0.,-1.));
#28318=DIRECTION('ref_axis',(1.,0.,1.20185167898973E-16));
#28319=DIRECTION('',(-1.,0.,-1.20185167898973E-16));
#28320=DIRECTION('',(0.,-1.,0.));
#28321=DIRECTION('',(1.,0.,1.20185167898973E-16));
#28322=DIRECTION('center_axis',(-0.866025403784439,0.,-0.5));
#28323=DIRECTION('ref_axis',(0.5,0.,-0.866025403784439));
#28324=DIRECTION('',(-0.5,0.,0.866025403784439));
#28325=DIRECTION('',(0.,-1.,0.));
#28326=DIRECTION('',(0.5,0.,-0.866025403784439));
#28327=DIRECTION('center_axis',(-0.866025403784439,0.,0.5));
#28328=DIRECTION('ref_axis',(-0.5,0.,-0.866025403784439));
#28329=DIRECTION('',(0.5,0.,0.866025403784439));
#28330=DIRECTION('',(0.,-1.,0.));
#28331=DIRECTION('',(-0.5,0.,-0.866025403784439));
#28332=DIRECTION('center_axis',(-2.40370335797945E-16,0.,1.));
#28333=DIRECTION('ref_axis',(-1.,0.,-2.40370335797945E-16));
#28334=DIRECTION('',(1.,0.,2.40370335797945E-16));
#28335=DIRECTION('',(0.,-1.,0.));
#28336=DIRECTION('',(-1.,0.,-2.40370335797945E-16));
#28337=DIRECTION('center_axis',(0.866025403784439,0.,0.5));
#28338=DIRECTION('ref_axis',(-0.5,0.,0.866025403784439));
#28339=DIRECTION('',(0.5,0.,-0.866025403784439));
#28340=DIRECTION('',(-0.5,0.,0.866025403784439));
#28341=DIRECTION('center_axis',(0.,1.,0.));
#28342=DIRECTION('ref_axis',(1.,0.,0.));
#28343=DIRECTION('center_axis',(0.,-1.,0.));
#28344=DIRECTION('ref_axis',(0.,0.,-1.));
#28345=DIRECTION('center_axis',(0.,1.,0.));
#28346=DIRECTION('ref_axis',(1.,0.,0.));
#28347=DIRECTION('center_axis',(0.,1.,0.));
#28348=DIRECTION('ref_axis',(1.,0.,0.));
#28349=DIRECTION('center_axis',(0.,1.,0.));
#28350=DIRECTION('ref_axis',(1.,0.,0.));
#28351=DIRECTION('center_axis',(0.,1.,0.));
#28352=DIRECTION('ref_axis',(1.,0.,0.));
#28353=DIRECTION('',(0.,-1.,0.));
#28354=DIRECTION('center_axis',(0.,1.,0.));
#28355=DIRECTION('ref_axis',(1.,0.,0.));
#28356=DIRECTION('center_axis',(0.,1.,0.));
#28357=DIRECTION('ref_axis',(1.,0.,0.));
#28358=DIRECTION('center_axis',(0.,1.,0.));
#28359=DIRECTION('ref_axis',(0.,0.,1.));
#28360=DIRECTION('center_axis',(0.,-1.,0.));
#28361=DIRECTION('ref_axis',(1.,0.,0.));
#28362=DIRECTION('center_axis',(0.,-1.,0.));
#28363=DIRECTION('ref_axis',(1.,0.,0.));
#28364=DIRECTION('center_axis',(0.,-1.,0.));
#28365=DIRECTION('ref_axis',(1.,0.,0.));
#28366=DIRECTION('',(0.707106781186548,0.707106781186547,8.65956056235493E-17));
#28367=DIRECTION('center_axis',(0.,-1.,0.));
#28368=DIRECTION('ref_axis',(1.,0.,0.));
#28369=DIRECTION('center_axis',(0.,-1.,0.));
#28370=DIRECTION('ref_axis',(1.,0.,0.));
#28371=DIRECTION('',(0.,1.,0.));
#28372=DIRECTION('center_axis',(0.,1.,0.));
#28373=DIRECTION('ref_axis',(1.,0.,0.));
#28374=DIRECTION('center_axis',(0.,-1.,0.));
#28375=DIRECTION('ref_axis',(1.,0.,0.));
#28376=DIRECTION('',(-0.707106781186547,0.707106781186548,-8.65956056235493E-17));
#28377=DIRECTION('center_axis',(0.,-1.,0.));
#28378=DIRECTION('ref_axis',(0.,0.,-1.));
#28379=DIRECTION('center_axis',(0.,-1.,0.));
#28380=DIRECTION('ref_axis',(1.,0.,0.));
#28381=DIRECTION('center_axis',(0.,1.,0.));
#28382=DIRECTION('ref_axis',(1.,0.,0.));
#28383=DIRECTION('center_axis',(0.,1.,0.));
#28384=DIRECTION('ref_axis',(1.,0.,0.));
#28385=DIRECTION('',(-0.447213595499958,0.894427190999916,-5.47678698264203E-17));
#28386=DIRECTION('center_axis',(0.,-1.,0.));
#28387=DIRECTION('ref_axis',(1.,0.,0.));
#28388=DIRECTION('',(0.,1.,0.));
#35183=CARTESIAN_POINT('',(0.,0.,0.));
#35184=CARTESIAN_POINT('Origin',(0.115470053837925,-0.5,-0.2));
#35185=CARTESIAN_POINT('',(0.23094010767585,-0.5,0.));
#35186=CARTESIAN_POINT('',(0.115470053837925,-0.5,-0.2));
#35187=CARTESIAN_POINT('',(0.23094010767585,-0.5,0.));
#35188=CARTESIAN_POINT('',(0.115470053837925,-0.8,-0.2));
#35189=CARTESIAN_POINT('',(0.115470053837925,-0.5,-0.2));
#35190=CARTESIAN_POINT('',(0.23094010767585,-0.8,0.));
#35191=CARTESIAN_POINT('',(0.23094010767585,-0.8,0.));
#35192=CARTESIAN_POINT('',(0.23094010767585,-0.5,0.));
#35193=CARTESIAN_POINT('Origin',(-0.115470053837925,-0.5,-0.2));
#35194=CARTESIAN_POINT('',(-0.115470053837925,-0.5,-0.2));
#35195=CARTESIAN_POINT('',(0.115470053837925,-0.5,-0.2));
#35196=CARTESIAN_POINT('',(-0.115470053837925,-0.8,-0.2));
#35197=CARTESIAN_POINT('',(-0.115470053837925,-0.5,-0.2));
#35198=CARTESIAN_POINT('',(0.115470053837925,-0.8,-0.2));
#35199=CARTESIAN_POINT('Origin',(-0.23094010767585,-0.5,-2.77555756156289E-17));
#35200=CARTESIAN_POINT('',(-0.23094010767585,-0.5,-2.82820063659975E-17));
#35201=CARTESIAN_POINT('',(-0.115470053837925,-0.5,-0.2));
#35202=CARTESIAN_POINT('',(-0.23094010767585,-0.8,-2.77555756156289E-17));
#35203=CARTESIAN_POINT('',(-0.23094010767585,-0.5,-2.82820063659975E-17));
#35204=CARTESIAN_POINT('',(-0.115470053837925,-0.8,-0.2));
#35205=CARTESIAN_POINT('Origin',(-0.115470053837925,-0.5,0.2));
#35206=CARTESIAN_POINT('',(-0.115470053837925,-0.5,0.2));
#35207=CARTESIAN_POINT('',(-0.23094010767585,-0.5,-2.82820063659975E-17));
#35208=CARTESIAN_POINT('',(-0.115470053837925,-0.8,0.2));
#35209=CARTESIAN_POINT('',(-0.115470053837925,-0.5,0.2));
#35210=CARTESIAN_POINT('',(-0.23094010767585,-0.8,-2.82820063659975E-17));
#35211=CARTESIAN_POINT('Origin',(0.115470053837925,-0.5,0.2));
#35212=CARTESIAN_POINT('',(0.115470053837925,-0.5,0.2));
#35213=CARTESIAN_POINT('',(-0.115470053837925,-0.5,0.2));
#35214=CARTESIAN_POINT('',(0.115470053837925,-0.8,0.2));
#35215=CARTESIAN_POINT('',(0.115470053837925,-0.5,0.2));
#35216=CARTESIAN_POINT('',(-0.115470053837925,-0.8,0.2));
#35217=CARTESIAN_POINT('Origin',(0.23094010767585,-0.5,0.));
#35218=CARTESIAN_POINT('',(0.115470053837925,-0.5,0.2));
#35219=CARTESIAN_POINT('',(0.115470053837925,-0.8,0.2));
#35220=CARTESIAN_POINT('Origin',(0.,-0.5,0.));
#35221=CARTESIAN_POINT('Origin',(0.,-0.8,0.));
#35222=CARTESIAN_POINT('Origin',(0.,-1.9,0.));
#35223=CARTESIAN_POINT('',(-0.25,-1.9,3.06161699786838E-17));
#35224=CARTESIAN_POINT('Origin',(0.,-1.9,0.));
#35225=CARTESIAN_POINT('',(-0.24505,-1.9,3.00099698131059E-17));
#35226=CARTESIAN_POINT('Origin',(0.,-1.9,0.));
#35227=CARTESIAN_POINT('Origin',(0.,-3.,0.));
#35228=CARTESIAN_POINT('',(-0.25,-3.,3.06161699786838E-17));
#35229=CARTESIAN_POINT('',(-0.25,-3.,3.06161699786838E-17));
#35230=CARTESIAN_POINT('Origin',(0.,-3.,0.));
#35231=CARTESIAN_POINT('Origin',(0.,-3.,0.));
#35232=CARTESIAN_POINT('Origin',(0.375,0.5,0.));
#35233=CARTESIAN_POINT('',(-0.375,0.5,-4.59242549680257E-17));
#35234=CARTESIAN_POINT('Origin',(0.,0.5,0.));
#35235=CARTESIAN_POINT('Origin',(0.,0.475,0.));
#35236=CARTESIAN_POINT('',(-0.425,0.45,-5.20474889637625E-17));
#35237=CARTESIAN_POINT('Origin',(0.,0.45,0.));
#35238=CARTESIAN_POINT('',(-0.4,0.475,-4.89858719658941E-17));
#35239=CARTESIAN_POINT('Origin',(0.,0.24,0.));
#35240=CARTESIAN_POINT('',(-0.425,0.0299999999999998,-5.20474889637625E-17));
#35241=CARTESIAN_POINT('Origin',(0.,0.0299999999999998,0.));
#35242=CARTESIAN_POINT('',(-0.425,0.24,-5.20474889637625E-17));
#35243=CARTESIAN_POINT('Origin',(0.,0.0150000000000001,0.));
#35244=CARTESIAN_POINT('',(-0.395,4.85722573273506E-17,-4.83735485663204E-17));
#35245=CARTESIAN_POINT('Origin',(0.,0.,0.));
#35246=CARTESIAN_POINT('',(-0.41,0.0150000000000001,-5.02105187650415E-17));
#35247=CARTESIAN_POINT('Origin',(0.27,0.,0.));
#35248=CARTESIAN_POINT('',(-0.27,0.,-3.30654635769785E-17));
#35249=CARTESIAN_POINT('Origin',(0.,0.,0.));
#35250=CARTESIAN_POINT('Origin',(0.,-0.02,0.));
#35251=CARTESIAN_POINT('',(-0.24505,-0.0498999999999999,3.00099698131059E-17));
#35252=CARTESIAN_POINT('Origin',(0.,-0.0498999999999999,0.));
#35253=CARTESIAN_POINT('',(-0.26,-0.02,-3.18408167778312E-17));
#35254=CARTESIAN_POINT('Origin',(0.,-0.995,0.));
#35255=CARTESIAN_POINT('',(-0.24505,-0.995,-3.00099698131059E-17));
#62822=UNCERTAINTY_MEASURE_WITH_UNIT(LENGTH_MEASURE(0.001),#62985,
'DISTANCE_ACCURACY_VALUE',
'Maximum model space distance between geometric entities at asserted c
onnectivities');
#62885=UNCERTAINTY_MEASURE_WITH_UNIT(LENGTH_MEASURE(0.001),#62985,
'DISTANCE_ACCURACY_VALUE',
'Maximum model space distance between geometric entities at asserted c
onnectivities');
#62921=(
GEOMETRIC_REPRESENTATION_CONTEXT(3)
GLOBAL_UNCERTAINTY_ASSIGNED_CONTEXT((#62822))
GLOBAL_UNIT_ASSIGNED_CONTEXT((#62985,#62987,#62988))
REPRESENTATION_CONTEXT('','3D')
);
#62984=(
GEOMETRIC_REPRESENTATION_CONTEXT(3)
GLOBAL_UNCERTAINTY_ASSIGNED_CONTEXT((#62885))
GLOBAL_UNIT_ASSIGNED_CONTEXT((#62985,#62987,#62988))
REPRESENTATION_CONTEXT('','3D')
);
#62985=(
LENGTH_UNIT()
NAMED_UNIT(*)
SI_UNIT(.CENTI.,.METRE.)
);
#62987=(
NAMED_UNIT(*)
PLANE_ANGLE_UNIT()
SI_UNIT($,.RADIAN.)
);
#62988=(
NAMED_UNIT(*)
SI_UNIT($,.STERADIAN.)
SOLID_ANGLE_UNIT()
);
#63024=SHAPE_DEFINITION_REPRESENTATION(#63135,#63384);
#63135=PRODUCT_DEFINITION_SHAPE('',$,#63483);
#63384=SHAPE_REPRESENTATION('',(#24724),#62921);
#63447=PRODUCT_DEFINITION_CONTEXT('part definition',#63743,'design');
#63483=PRODUCT_DEFINITION('M5x30 frame screw','M5x30 frame screw',#63581,
#63447);
#63581=PRODUCT_DEFINITION_FORMATION('',$,#63780);
#63743=APPLICATION_CONTEXT(
'Core Data for Automotive Mechanical Design Process');
#63744=PRODUCT_CONTEXT('part definition',#63743,'mechanical');
#63780=PRODUCT('M5x30 frame screw','M5x30 frame screw',
'M5x30 frame screw',(#63744));
#63913=COLOUR_RGB('Black',0.12,0.14,0.17);
#63914=FILL_AREA_STYLE_COLOUR('',#63913);
#63915=FILL_AREA_STYLE('',(#63914));
#63916=SURFACE_STYLE_FILL_AREA(#63915);
#63917=SURFACE_SIDE_STYLE('',(#63916));
#63918=SURFACE_STYLE_USAGE(.BOTH.,#63917);
#63919=PRESENTATION_STYLE_ASSIGNMENT((#63918));
ENDSEC;
END-ISO-10303-21;
